ISO-10303-21;
HEADER;
FILE_DESCRIPTION (('STEP AP214'),
    '1' );
FILE_NAME ('single rail^MAS-188.step',
    '2026-10-24T11:01:53',
    ( '' ),
    ( '' ),
    'SwSTEP 2.0',
    'SolidWorks 2026',
    '' );
FILE_SCHEMA (( 'AUTOMOTIVE_DESIGN' ));
ENDSEC;

DATA;
#25=DIRECTION ( 'NONE',  ( 0.000000000000000000, 0.000000000000000000, 1.000000000000000000 ) ) ;
#40=DIRECTION ( 'NONE',  ( 1.000000000000000000, 0.000000000000000000, 0.000000000000000000 ) ) ;
#57=ADVANCED_FACE ( 'NONE', ( #4416 ), #7068, .T. ) ;
#68=ORIENTED_EDGE ( 'NONE', *, *, #4489, .T. ) ;
#85=DIRECTION ( 'NONE',  ( 0.000000000000000000, 1.000000000000000000, 0.000000000000000000 ) ) ;
#142=CARTESIAN_POINT ( 'NONE',  ( 0.000000000000000000, 157.5000000000000284, 0.000000000000000000 ) ) ;
#189=EDGE_CURVE ( 'NONE', #7561, #1754, #4818, .T. ) ;
#191=FACE_OUTER_BOUND ( 'NONE', #6163, .T. ) ;
#193=CARTESIAN_POINT ( 'NONE',  ( -4.999999999999998224, 135.0000000000000000, 25.00000000000000000 ) ) ;
#239=DIRECTION ( 'NONE',  ( -0.000000000000000000, -0.000000000000000000, -1.000000000000000000 ) ) ;
#252=ORIENTED_EDGE ( 'NONE', *, *, #8466, .T. ) ;
#266=CARTESIAN_POINT ( 'NONE',  ( -20.00000000000000000, 135.0000000000000000, 40.00000000000000000 ) ) ;
#271=ORIENTED_EDGE ( 'NONE', *, *, #4539, .T. ) ;
#276=LINE ( 'NONE', #6936, #1165 ) ;
#300=PRODUCT_DEFINITION_FORMATION_WITH_SPECIFIED_SOURCE ( 'ANY', '', #7393, .NOT_KNOWN. ) ;
#343=DIRECTION ( 'NONE',  ( -0.000000000000000000, -0.000000000000000000, 1.000000000000000000 ) ) ;
#354=CIRCLE ( 'NONE', #2031, 2.649999999999993694 ) ;
#358=ORIENTED_EDGE ( 'NONE', *, *, #189, .F. ) ;
#393=ADVANCED_FACE ( 'NONE', ( #1075, #7701 ), #3728, .F. ) ;
#394=PRESENTATION_STYLE_ASSIGNMENT (( #714 ) ) ;
#403=LINE ( 'NONE', #6405, #2228 ) ;
#405=( LENGTH_UNIT ( ) NAMED_UNIT ( * ) SI_UNIT ( .MILLI., .METRE. ) );
#436=EDGE_LOOP ( 'NONE', ( #8463, #5581, #6802, #4042 ) ) ;
#447=( NAMED_UNIT ( * ) SI_UNIT ( $, .STERADIAN. ) SOLID_ANGLE_UNIT ( ) );
#464=DIRECTION ( 'NONE',  ( 0.000000000000000000, 0.000000000000000000, 1.000000000000000000 ) ) ;
#468=CARTESIAN_POINT ( 'NONE',  ( -4.999999999999998224, 134.9989999999999952, 25.00000000000000000 ) ) ;
#474=ORIENTED_EDGE ( 'NONE', *, *, #4612, .F. ) ;
#477=CARTESIAN_POINT ( 'NONE',  ( -20.00000000000000000, 140.0000000000000000, 4.999999999999997335 ) ) ;
#512=ADVANCED_FACE ( 'NONE', ( #5794, #3887 ), #6531, .T. ) ;
#530=VERTEX_POINT ( 'NONE', #8502 ) ;
#582=LINE ( 'NONE', #6341, #7776 ) ;
#593=CARTESIAN_POINT ( 'NONE',  ( 5.000000000000000000, 135.0000000000000000, 25.00000000000000000 ) ) ;
#594=AXIS2_PLACEMENT_3D ( 'NONE', #3123, #464, #5764 ) ;
#607=EDGE_CURVE ( 'NONE', #3740, #2174, #5920, .T. ) ;
#620=DIRECTION ( 'NONE',  ( 0.000000000000000000, 0.000000000000000000, -1.000000000000000000 ) ) ;
#632=AXIS2_PLACEMENT_3D ( 'NONE', #468, #1079, #5768 ) ;
#633=ORIENTED_EDGE ( 'NONE', *, *, #2383, .T. ) ;
#668=EDGE_CURVE ( 'NONE', #3213, #3699, #4707, .T. ) ;
#693=VECTOR ( 'NONE', #5102, 1000.000000000000000 ) ;
#707=DIRECTION ( 'NONE',  ( -0.000000000000000000, 1.000000000000000000, -0.000000000000000000 ) ) ;
#714=SURFACE_STYLE_USAGE ( .BOTH. , #6668 ) ;
#725=ORIENTED_EDGE ( 'NONE', *, *, #2747, .T. ) ;
#726=CARTESIAN_POINT ( 'NONE',  ( 20.00000000000000000, 135.0000000000000000, 40.00000000000000000 ) ) ;
#738=DIRECTION ( 'NONE',  ( 1.000000000000000000, 0.000000000000000000, 0.000000000000000000 ) ) ;
#791=EDGE_LOOP ( 'NONE', ( #358, #3547, #5822, #6456, #2085, #271 ) ) ;
#867=DIRECTION ( 'NONE',  ( 0.000000000000000000, 0.000000000000000000, -1.000000000000000000 ) ) ;
#872=SHAPE_REPRESENTATION ( 'single rail^MAS-188', ( #594 ), #4077 ) ;
#939=EDGE_CURVE ( 'NONE', #3102, #1905, #6485, .T. ) ;
#962=ORIENTED_EDGE ( 'NONE', *, *, #7523, .T. ) ;
#976=EDGE_CURVE ( 'NONE', #3444, #530, #354, .T. ) ;
#992=ORIENTED_EDGE ( 'NONE', *, *, #2383, .F. ) ;
#999=DIRECTION ( 'NONE',  ( -0.000000000000000000, -0.000000000000000000, 1.000000000000000000 ) ) ;
#1005=VECTOR ( 'NONE', #2734, 1000.000000000000000 ) ;
#1016=VECTOR ( 'NONE', #239, 1000.000000000000000 ) ;
#1024=VECTOR ( 'NONE', #8001, 1000.000000000000000 ) ;
#1036=ORIENTED_EDGE ( 'NONE', *, *, #1548, .T. ) ;
#1064=VECTOR ( 'NONE', #2605, 1000.000000000000000 ) ;
#1069=UNCERTAINTY_MEASURE_WITH_UNIT (LENGTH_MEASURE( 1.000000000000000082E-05 ), #4318, 'distance_accuracy_value', 'NONE');
#1075=FACE_BOUND ( 'NONE', #2339, .T. ) ;
#1079=DIRECTION ( 'NONE',  ( -0.000000000000000000, 0.000000000000000000, 1.000000000000000000 ) ) ;
#1081=APPLICATION_CONTEXT ( 'automotive_design' ) ;
#1104=DIRECTION ( 'NONE',  ( -0.000000000000000000, -0.000000000000000000, -1.000000000000000000 ) ) ;
#1110=CARTESIAN_POINT ( 'NONE',  ( -20.00000000000000000, 140.0000000000000000, 5.000000000000000000 ) ) ;
#1144=DIRECTION ( 'NONE',  ( -0.000000000000000000, -0.000000000000000000, 1.000000000000000000 ) ) ;
#1150=ORIENTED_EDGE ( 'NONE', *, *, #4489, .F. ) ;
#1159=CIRCLE ( 'NONE', #4764, 2.649999999999993694 ) ;
#1165=VECTOR ( 'NONE', #4331, 1000.000000000000000 ) ;
#1181=ADVANCED_FACE ( 'NONE', ( #6300, #2784 ), #6256, .F. ) ;
#1251=DIRECTION ( 'NONE',  ( -0.000000000000000000, 1.000000000000000000, -0.000000000000000000 ) ) ;
#1289=LINE ( 'NONE', #7341, #1064 ) ;
#1295=EDGE_LOOP ( 'NONE', ( #4425, #5553, #1036, #7577, #5292, #7395 ) ) ;
#1338=FACE_OUTER_BOUND ( 'NONE', #4464, .T. ) ;
#1342=( GEOMETRIC_REPRESENTATION_CONTEXT ( 3 ) GLOBAL_UNCERTAINTY_ASSIGNED_CONTEXT ( ( #4950 ) ) GLOBAL_UNIT_ASSIGNED_CONTEXT ( ( #405, #2467, #447 ) ) REPRESENTATION_CONTEXT ( 'NONE', 'WORKASPACE' ) );
#1366=SURFACE_STYLE_FILL_AREA ( #7334 ) ;
#1373=VECTOR ( 'NONE', #7481, 1000.000000000000000 ) ;
#1397=DIRECTION ( 'NONE',  ( 0.000000000000000000, -1.000000000000000000, 0.000000000000000000 ) ) ;
#1400=FACE_BOUND ( 'NONE', #6464, .T. ) ;
#1426=VERTEX_POINT ( 'NONE', #3735 ) ;
#1440=ORIENTED_EDGE ( 'NONE', *, *, #6089, .T. ) ;
#1476=ADVANCED_BREP_SHAPE_REPRESENTATION ( '', ( #2129, #594 ), #4077 ) ;
#1482=ORIENTED_EDGE ( 'NONE', *, *, #2411, .T. ) ;
#1484=CARTESIAN_POINT ( 'NONE',  ( 4.999999999999997335, 135.0000000000000000, 25.00000000000000000 ) ) ;
#1526=EDGE_LOOP ( 'NONE', ( #1440, #3470, #992, #6874 ) ) ;
#1536=AXIS2_PLACEMENT_3D ( 'NONE', #2377, #2507, #7102 ) ;
#1548=EDGE_CURVE ( 'NONE', #1426, #6694, #1289, .T. ) ;
#1550=DIRECTION ( 'NONE',  ( 0.000000000000000000, 1.000000000000000000, 0.000000000000000000 ) ) ;
#1642=VECTOR ( 'NONE', #2175, 1000.000000000000000 ) ;
#1662=CARTESIAN_POINT ( 'NONE',  ( 0.000000000000000000, 157.5000000000000284, 5.000000000000000000 ) ) ;
#1665=ADVANCED_FACE ( 'NONE', ( #191 ), #2812, .T. ) ;
#1681=CARTESIAN_POINT ( 'NONE',  ( 5.000000000000000000, 134.9989999999999952, 25.00000000000000000 ) ) ;
#1754=VERTEX_POINT ( 'NONE', #5801 ) ;
#1760=CARTESIAN_POINT ( 'NONE',  ( 0.000000000000000000, 157.5000000000000284, 5.000000000000000888 ) ) ;
#1789=ORIENTED_EDGE ( 'NONE', *, *, #5178, .T. ) ;
#1831=ORIENTED_EDGE ( 'NONE', *, *, #607, .T. ) ;
#1837=CARTESIAN_POINT ( 'NONE',  ( -20.00000000000000000, 140.0000000000000000, 40.00000000000000000 ) ) ;
#1861=COLOUR_RGB ( '',0.8941176470588234615, 0.8941176470588234615, 0.8941176470588234615 ) ;
#1877=DIRECTION ( 'NONE',  ( -0.000000000000000000, -0.000000000000000000, -1.000000000000000000 ) ) ;
#1895=EDGE_CURVE ( 'NONE', #2697, #6761, #3946, .T. ) ;
#1899=LINE ( 'NONE', #3456, #7260 ) ;
#1905=VERTEX_POINT ( 'NONE', #4541 ) ;
#1918=ORIENTED_EDGE ( 'NONE', *, *, #3084, .F. ) ;
#1928=VECTOR ( 'NONE', #40, 1000.000000000000000 ) ;
#1955=ORIENTED_EDGE ( 'NONE', *, *, #976, .F. ) ;
#1958=CARTESIAN_POINT ( 'NONE',  ( -20.00000000000000000, 175.0000000000000284, 5.000000000000000000 ) ) ;
#1968=CARTESIAN_POINT ( 'NONE',  ( -4.999999999999998224, 134.9989999999999952, 25.00000000000000000 ) ) ;
#1971=ORIENTED_EDGE ( 'NONE', *, *, #2809, .T. ) ;
#2000=LINE ( 'NONE', #3910, #8403 ) ;
#2005=( GEOMETRIC_REPRESENTATION_CONTEXT ( 3 ) GLOBAL_UNCERTAINTY_ASSIGNED_CONTEXT ( ( #3765 ) ) GLOBAL_UNIT_ASSIGNED_CONTEXT ( ( #3146, #8499, #3795 ) ) REPRESENTATION_CONTEXT ( 'NONE', 'WORKASPACE' ) );
#2031=AXIS2_PLACEMENT_3D ( 'NONE', #7843, #4482, #3058 ) ;
#2082=CARTESIAN_POINT ( 'NONE',  ( -20.00000000000000000, 140.0000000000000000, 0.000000000000000000 ) ) ;
#2085=ORIENTED_EDGE ( 'NONE', *, *, #6319, .T. ) ;
#2099=ORIENTED_EDGE ( 'NONE', *, *, #7670, .T. ) ;
#2129=MANIFOLD_SOLID_BREP ( 'M5 Clearance Hole1', #3987 ) ;
#2140=EDGE_LOOP ( 'NONE', ( #2982, #4100, #4359, #5653 ) ) ;
#2173=CARTESIAN_POINT ( 'NONE',  ( -2.649999999999993694, 157.5000000000000284, 5.000000000000000000 ) ) ;
#2174=VERTEX_POINT ( 'NONE', #5105 ) ;
#2175=DIRECTION ( 'NONE',  ( 1.000000000000000000, 0.000000000000000000, 0.000000000000000000 ) ) ;
#2180=LINE ( 'NONE', #2788, #7543 ) ;
#2209=DIRECTION ( 'NONE',  ( 0.000000000000000000, 1.000000000000000000, 0.000000000000000000 ) ) ;
#2228=VECTOR ( 'NONE', #1104, 1000.000000000000000 ) ;
#2235=( NAMED_UNIT ( * ) PLANE_ANGLE_UNIT ( ) SI_UNIT ( $, .RADIAN. ) );
#2268=DIRECTION ( 'NONE',  ( 1.734723475976807341E-16, 0.000000000000000000, -1.000000000000000000 ) ) ;
#2295=EDGE_CURVE ( 'NONE', #1754, #3213, #6782, .T. ) ;
#2339=EDGE_LOOP ( 'NONE', ( #3332, #2695, #2341, #6159 ) ) ;
#2341=ORIENTED_EDGE ( 'NONE', *, *, #2411, .F. ) ;
#2377=CARTESIAN_POINT ( 'NONE',  ( 20.00000000000000000, 175.0000000000000284, 5.000000000000000000 ) ) ;
#2383=EDGE_CURVE ( 'NONE', #5788, #1426, #7404, .T. ) ;
#2409=EDGE_CURVE ( 'NONE', #2174, #3740, #7888, .T. ) ;
#2411=EDGE_CURVE ( 'NONE', #5372, #8533, #2622, .T. ) ;
#2424=LINE ( 'NONE', #3193, #2926 ) ;
#2436=VECTOR ( 'NONE', #5675, 1000.000000000000000 ) ;
#2467=( NAMED_UNIT ( * ) PLANE_ANGLE_UNIT ( ) SI_UNIT ( $, .RADIAN. ) );
#2507=DIRECTION ( 'NONE',  ( 1.000000000000000000, 0.000000000000000000, -0.000000000000000000 ) ) ;
#2538=ORIENTED_EDGE ( 'NONE', *, *, #4539, .F. ) ;
#2546=DIRECTION ( 'NONE',  ( 0.000000000000000000, 1.000000000000000000, 0.000000000000000000 ) ) ;
#2583=CARTESIAN_POINT ( 'NONE',  ( 0.000000000000000000, 157.5000000000000284, 5.000000000000000888 ) ) ;
#2584=CARTESIAN_POINT ( 'NONE',  ( -2.649999999999993694, 157.5000000000000284, 0.000000000000000000 ) ) ;
#2591=CARTESIAN_POINT ( 'NONE',  ( 5.000000000000001776, 134.9989999999999952, 15.00000000000000355 ) ) ;
#2605=DIRECTION ( 'NONE',  ( 0.000000000000000000, -1.000000000000000000, 0.000000000000000000 ) ) ;
#2616=DIRECTION ( 'NONE',  ( 0.000000000000000000, 0.000000000000000000, -1.000000000000000000 ) ) ;
#2622=LINE ( 'NONE', #5354, #6511 ) ;
#2631=AXIS2_PLACEMENT_3D ( 'NONE', #3409, #85, #8076 ) ;
#2642=DIRECTION ( 'NONE',  ( 1.000000000000000000, 0.000000000000000000, 0.000000000000000000 ) ) ;
#2647=CARTESIAN_POINT ( 'NONE',  ( -20.00000000000000000, 135.0000000000000000, 40.00000000000000000 ) ) ;
#2674=DIRECTION ( 'NONE',  ( -1.000000000000000000, 0.000000000000000000, 0.000000000000000000 ) ) ;
#2695=ORIENTED_EDGE ( 'NONE', *, *, #2851, .F. ) ;
#2697=VERTEX_POINT ( 'NONE', #1837 ) ;
#2729=AXIS2_PLACEMENT_3D ( 'NONE', #1110, #3762, #4731 ) ;
#2734=DIRECTION ( 'NONE',  ( 0.000000000000000000, -1.000000000000000000, 0.000000000000000000 ) ) ;
#2747=EDGE_CURVE ( 'NONE', #8315, #3043, #5867, .T. ) ;
#2767=ORIENTED_EDGE ( 'NONE', *, *, #5228, .F. ) ;
#2784=FACE_BOUND ( 'NONE', #6488, .T. ) ;
#2788=CARTESIAN_POINT ( 'NONE',  ( 20.00000000000000000, 175.0000000000000284, 5.000000000000000000 ) ) ;
#2796=PLANE ( 'NONE',  #2631 ) ;
#2809=EDGE_CURVE ( 'NONE', #7561, #3699, #4604, .T. ) ;
#2812=PLANE ( 'NONE',  #3422 ) ;
#2828=CARTESIAN_POINT ( 'NONE',  ( 5.000000000000000000, 140.0000000000000000, 25.00000000000000000 ) ) ;
#2851=EDGE_CURVE ( 'NONE', #8533, #6097, #3353, .T. ) ;
#2896=EDGE_CURVE ( 'NONE', #3043, #1905, #6822, .T. ) ;
#2906=CARTESIAN_POINT ( 'NONE',  ( -20.00000000000000000, 175.0000000000000284, 5.000000000000000000 ) ) ;
#2926=VECTOR ( 'NONE', #2546, 1000.000000000000000 ) ;
#2927=EDGE_CURVE ( 'NONE', #3444, #2174, #6780, .T. ) ;
#2982=ORIENTED_EDGE ( 'NONE', *, *, #8547, .T. ) ;
#3027=EDGE_LOOP ( 'NONE', ( #4223, #3721, #5454, #4589 ) ) ;
#3030=AXIS2_PLACEMENT_3D ( 'NONE', #2583, #8591, #3975 ) ;
#3043=VERTEX_POINT ( 'NONE', #7662 ) ;
#3047=DIRECTION ( 'NONE',  ( -1.000000000000000000, 0.000000000000000000, 0.000000000000000000 ) ) ;
#3051=FACE_OUTER_BOUND ( 'NONE', #2140, .T. ) ;
#3058=DIRECTION ( 'NONE',  ( -1.000000000000000000, 0.000000000000000000, 0.000000000000000000 ) ) ;
#3084=EDGE_CURVE ( 'NONE', #1905, #8421, #582, .T. ) ;
#3102=VERTEX_POINT ( 'NONE', #4390 ) ;
#3108=LINE ( 'NONE', #4368, #693 ) ;
#3123=CARTESIAN_POINT ( 'NONE',  ( 0.000000000000000000, 0.000000000000000000, 0.000000000000000000 ) ) ;
#3146=( LENGTH_UNIT ( ) NAMED_UNIT ( * ) SI_UNIT ( .MILLI., .METRE. ) );
#3151=DIRECTION ( 'NONE',  ( 1.000000000000000000, 0.000000000000000000, 0.000000000000000000 ) ) ;
#3152=PLANE ( 'NONE',  #1536 ) ;
#3193=CARTESIAN_POINT ( 'NONE',  ( -20.00000000000000000, 135.0000000000000000, 40.00000000000000000 ) ) ;
#3213=VERTEX_POINT ( 'NONE', #6095 ) ;
#3215=PRODUCT_CONTEXT ( 'NONE', #7764, 'mechanical' ) ;
#3237=CARTESIAN_POINT ( 'NONE',  ( -20.00000000000000000, 140.0000000000000000, 40.00000000000000000 ) ) ;
#3299=LINE ( 'NONE', #2647, #5046 ) ;
#3311=ORIENTED_EDGE ( 'NONE', *, *, #5228, .T. ) ;
#3332=ORIENTED_EDGE ( 'NONE', *, *, #7523, .F. ) ;
#3353=LINE ( 'NONE', #5991, #7642 ) ;
#3409=CARTESIAN_POINT ( 'NONE',  ( -20.00000000000000000, 140.0000000000000000, 40.00000000000000000 ) ) ;
#3422=AXIS2_PLACEMENT_3D ( 'NONE', #5461, #1550, #3425 ) ;
#3425=DIRECTION ( 'NONE',  ( 0.000000000000000000, -0.000000000000000000, 1.000000000000000000 ) ) ;
#3426=EDGE_CURVE ( 'NONE', #2697, #4430, #5877, .T. ) ;
#3439=PRODUCT_DEFINITION_SHAPE ( 'NONE', 'NONE',  #4792 ) ;
#3444=VERTEX_POINT ( 'NONE', #2584 ) ;
#3456=CARTESIAN_POINT ( 'NONE',  ( 5.000000000000000000, 134.9989999999999952, 25.00000000000000000 ) ) ;
#3470=ORIENTED_EDGE ( 'NONE', *, *, #1548, .F. ) ;
#3475=SHAPE_DEFINITION_REPRESENTATION ( #3439, #872 ) ;
#3547=ORIENTED_EDGE ( 'NONE', *, *, #4213, .F. ) ;
#3610=ADVANCED_FACE ( 'NONE', ( #7406 ), #5356, .F. ) ;
#3668=ORIENTED_EDGE ( 'NONE', *, *, #939, .T. ) ;
#3696=ADVANCED_FACE ( 'NONE', ( #1400, #6702 ), #2796, .T. ) ;
#3699=VERTEX_POINT ( 'NONE', #4573 ) ;
#3721=ORIENTED_EDGE ( 'NONE', *, *, #2809, .F. ) ;
#3722=DIRECTION ( 'NONE',  ( 1.734723475976807587E-16, 0.000000000000000000, -1.000000000000000000 ) ) ;
#3728=PLANE ( 'NONE',  #7317 ) ;
#3735=CARTESIAN_POINT ( 'NONE',  ( 20.00000000000000000, 175.0000000000000284, 5.000000000000000000 ) ) ;
#3740=VERTEX_POINT ( 'NONE', #8158 ) ;
#3741=ORIENTED_EDGE ( 'NONE', *, *, #1895, .F. ) ;
#3744=VECTOR ( 'NONE', #7021, 1000.000000000000000 ) ;
#3751=AXIS2_PLACEMENT_3D ( 'NONE', #2591, #5234, #2674 ) ;
#3762=DIRECTION ( 'NONE',  ( -1.000000000000000000, 0.000000000000000000, 0.000000000000000000 ) ) ;
#3765=UNCERTAINTY_MEASURE_WITH_UNIT (LENGTH_MEASURE( 1.000000000000000082E-05 ), #3146, 'distance_accuracy_value', 'NONE');
#3781=ORIENTED_EDGE ( 'NONE', *, *, #976, .T. ) ;
#3784=CARTESIAN_POINT ( 'NONE',  ( 0.000000000000000000, 157.5000000000000284, 5.000000000000000000 ) ) ;
#3795=( NAMED_UNIT ( * ) SI_UNIT ( $, .STERADIAN. ) SOLID_ANGLE_UNIT ( ) );
#3852=AXIS2_PLACEMENT_3D ( 'NONE', #4570, #8380, #6451 ) ;
#3887=FACE_OUTER_BOUND ( 'NONE', #3027, .T. ) ;
#3910=CARTESIAN_POINT ( 'NONE',  ( -4.999999999999998224, 134.9989999999999952, 15.00000000000000355 ) ) ;
#3912=ADVANCED_FACE ( 'NONE', ( #6625 ), #4581, .F. ) ;
#3946=LINE ( 'NONE', #6586, #7604 ) ;
#3951=CARTESIAN_POINT ( 'NONE',  ( -20.00000000000000000, 140.0000000000000000, 5.000000000000000000 ) ) ;
#3963=ORIENTED_EDGE ( 'NONE', *, *, #8547, .F. ) ;
#3975=DIRECTION ( 'NONE',  ( 1.000000000000000000, 0.000000000000000000, 0.000000000000000000 ) ) ;
#3987=CLOSED_SHELL ( 'NONE', ( #4357, #1181, #4197, #1665, #57, #512, #3696, #393, #3610, #5701, #3912, #6378, #5921, #5566 ) ) ;
#4005=CARTESIAN_POINT ( 'NONE',  ( -4.999999999999998224, 134.9989999999999952, 15.00000000000000355 ) ) ;
#4008=DIRECTION ( 'NONE',  ( 1.000000000000000000, 0.000000000000000000, 0.000000000000000000 ) ) ;
#4032=CARTESIAN_POINT ( 'NONE',  ( 5.000000000000001776, 135.0000000000000000, 15.00000000000000355 ) ) ;
#4042=ORIENTED_EDGE ( 'NONE', *, *, #939, .F. ) ;
#4077=( GEOMETRIC_REPRESENTATION_CONTEXT ( 3 ) GLOBAL_UNCERTAINTY_ASSIGNED_CONTEXT ( ( #1069 ) ) GLOBAL_UNIT_ASSIGNED_CONTEXT ( ( #4318, #2235, #6228 ) ) REPRESENTATION_CONTEXT ( 'NONE', 'WORKASPACE' ) );
#4100=ORIENTED_EDGE ( 'NONE', *, *, #2927, .T. ) ;
#4111=VECTOR ( 'NONE', #8370, 1000.000000000000000 ) ;
#4197=ADVANCED_FACE ( 'NONE', ( #7850 ), #3152, .T. ) ;
#4206=DIRECTION ( 'NONE',  ( 0.000000000000000000, -0.000000000000000000, 1.000000000000000000 ) ) ;
#4213=EDGE_CURVE ( 'NONE', #8098, #7561, #3108, .T. ) ;
#4223=ORIENTED_EDGE ( 'NONE', *, *, #668, .T. ) ;
#4243=CARTESIAN_POINT ( 'NONE',  ( -20.00000000000000000, 140.0000000000000000, 5.000000000000000000 ) ) ;
#4258=VECTOR ( 'NONE', #7958, 1000.000000000000000 ) ;
#4265=CARTESIAN_POINT ( 'NONE',  ( -4.999999999999999112, 140.0000000000000000, 25.00000000000000000 ) ) ;
#4278=EDGE_CURVE ( 'NONE', #6761, #6694, #403, .T. ) ;
#4287=PLANE ( 'NONE',  #7842 ) ;
#4313=EDGE_CURVE ( 'NONE', #8098, #2697, #2424, .T. ) ;
#4318=( LENGTH_UNIT ( ) NAMED_UNIT ( * ) SI_UNIT ( .MILLI., .METRE. ) );
#4331=DIRECTION ( 'NONE',  ( -0.000000000000000000, -0.000000000000000000, 1.000000000000000000 ) ) ;
#4357=ADVANCED_FACE ( 'NONE', ( #3051 ), #5651, .F. ) ;
#4359=ORIENTED_EDGE ( 'NONE', *, *, #2409, .T. ) ;
#4368=CARTESIAN_POINT ( 'NONE',  ( -20.00000000000000000, 135.0000000000000000, 40.00000000000000000 ) ) ;
#4375=DIRECTION ( 'NONE',  ( 1.000000000000000000, 0.000000000000000000, 1.734723475976807587E-16 ) ) ;
#4390=CARTESIAN_POINT ( 'NONE',  ( 5.000000000000001776, 135.0000000000000000, 15.00000000000000355 ) ) ;
#4416=FACE_OUTER_BOUND ( 'NONE', #791, .T. ) ;
#4425=ORIENTED_EDGE ( 'NONE', *, *, #668, .F. ) ;
#4430=VERTEX_POINT ( 'NONE', #477 ) ;
#4464=EDGE_LOOP ( 'NONE', ( #8258, #68, #1789, #2767 ) ) ;
#4482=DIRECTION ( 'NONE',  ( 0.000000000000000000, 0.000000000000000000, -1.000000000000000000 ) ) ;
#4489=EDGE_CURVE ( 'NONE', #6097, #8421, #2000, .T. ) ;
#4539=EDGE_CURVE ( 'NONE', #5788, #1754, #7916, .T. ) ;
#4541=CARTESIAN_POINT ( 'NONE',  ( 5.000000000000001776, 140.0000000000000000, 15.00000000000000355 ) ) ;
#4545=ORIENTED_EDGE ( 'NONE', *, *, #2927, .F. ) ;
#4546=DIRECTION ( 'NONE',  ( 1.000000000000000000, 0.000000000000000000, 0.000000000000000000 ) ) ;
#4570=CARTESIAN_POINT ( 'NONE',  ( 0.000000000000000000, 0.000000000000000000, 0.000000000000000000 ) ) ;
#4573=CARTESIAN_POINT ( 'NONE',  ( 20.00000000000000000, 135.0000000000000000, 0.000000000000000000 ) ) ;
#4581=PLANE ( 'NONE',  #3751 ) ;
#4589=ORIENTED_EDGE ( 'NONE', *, *, #2295, .T. ) ;
#4604=LINE ( 'NONE', #6563, #5396 ) ;
#4612=EDGE_CURVE ( 'NONE', #6761, #5082, #4819, .T. ) ;
#4629=MECHANICAL_DESIGN_GEOMETRIC_PRESENTATION_REPRESENTATION('',(#5185),#2005);
#4638=ORIENTED_EDGE ( 'NONE', *, *, #2409, .F. ) ;
#4672=FILL_AREA_STYLE_COLOUR ( '', #1861 ) ;
#4701=LINE ( 'NONE', #1968, #7969 ) ;
#4707=LINE ( 'NONE', #5398, #6343 ) ;
#4718=ORIENTED_EDGE ( 'NONE', *, *, #7913, .F. ) ;
#4731=DIRECTION ( 'NONE',  ( 0.000000000000000000, 0.000000000000000000, 1.000000000000000000 ) ) ;
#4764=AXIS2_PLACEMENT_3D ( 'NONE', #142, #6108, #6726 ) ;
#4792=PRODUCT_DEFINITION ( 'UNKNOWN', '', #300, #7866 ) ;
#4818=LINE ( 'NONE', #2082, #4258 ) ;
#4819=LINE ( 'NONE', #8182, #1005 ) ;
#4922=CARTESIAN_POINT ( 'NONE',  ( 20.00000000000000000, 140.0000000000000000, 5.000000000000000000 ) ) ;
#4950=UNCERTAINTY_MEASURE_WITH_UNIT (LENGTH_MEASURE( 1.000000000000000082E-05 ), #405, 'distance_accuracy_value', 'NONE');
#4952=FACE_OUTER_BOUND ( 'NONE', #5541, .T. ) ;
#4956=CARTESIAN_POINT ( 'NONE',  ( 0.000000000000000000, 0.000000000000000000, 5.000000000000000000 ) ) ;
#5017=ORIENTED_EDGE ( 'NONE', *, *, #607, .F. ) ;
#5046=VECTOR ( 'NONE', #5938, 1000.000000000000000 ) ;
#5082=VERTEX_POINT ( 'NONE', #6317 ) ;
#5084=DIRECTION ( 'NONE',  ( 1.000000000000000000, 0.000000000000000000, 0.000000000000000000 ) ) ;
#5095=ORIENTED_EDGE ( 'NONE', *, *, #4278, .T. ) ;
#5098=AXIS2_PLACEMENT_3D ( 'NONE', #1760, #1144, #3151 ) ;
#5102=DIRECTION ( 'NONE',  ( -0.000000000000000000, -0.000000000000000000, -1.000000000000000000 ) ) ;
#5105=CARTESIAN_POINT ( 'NONE',  ( -2.649999999999987477, 157.5000000000000284, 5.000000000000000888 ) ) ;
#5136=CARTESIAN_POINT ( 'NONE',  ( 5.000000000000001776, 134.9989999999999952, 15.00000000000000355 ) ) ;
#5138=EDGE_LOOP ( 'NONE', ( #4545, #3781, #2099, #1831 ) ) ;
#5178=EDGE_CURVE ( 'NONE', #8421, #8315, #5872, .T. ) ;
#5179=SHAPE_REPRESENTATION_RELATIONSHIP ( 'NONE' , 'NONE' ,  #872, #1476 ) ;
#5185=STYLED_ITEM ( 'NONE', ( #394 ), #1476 ) ;
#5211=ORIENTED_EDGE ( 'NONE', *, *, #8262, .T. ) ;
#5228=EDGE_CURVE ( 'NONE', #8533, #8315, #4701, .T. ) ;
#5234=DIRECTION ( 'NONE',  ( -0.000000000000000000, 0.000000000000000000, -1.000000000000000000 ) ) ;
#5264=DIRECTION ( 'NONE',  ( -1.000000000000000000, 0.000000000000000000, -0.000000000000000000 ) ) ;
#5292=ORIENTED_EDGE ( 'NONE', *, *, #4612, .T. ) ;
#5354=CARTESIAN_POINT ( 'NONE',  ( -4.999999999999998224, 135.0000000000000000, 25.00000000000000000 ) ) ;
#5356=PLANE ( 'NONE',  #7922 ) ;
#5372=VERTEX_POINT ( 'NONE', #1484 ) ;
#5396=VECTOR ( 'NONE', #4008, 1000.000000000000000 ) ;
#5398=CARTESIAN_POINT ( 'NONE',  ( 20.00000000000000000, 175.0000000000000284, 0.000000000000000000 ) ) ;
#5433=DIRECTION ( 'NONE',  ( -0.000000000000000000, -0.000000000000000000, -1.000000000000000000 ) ) ;
#5454=ORIENTED_EDGE ( 'NONE', *, *, #189, .T. ) ;
#5461=CARTESIAN_POINT ( 'NONE',  ( -20.00000000000000000, 175.0000000000000284, 5.000000000000000000 ) ) ;
#5468=ORIENTED_EDGE ( 'NONE', *, *, #4313, .F. ) ;
#5509=CARTESIAN_POINT ( 'NONE',  ( -20.00000000000000000, 135.0000000000000000, 40.00000000000000000 ) ) ;
#5512=ORIENTED_EDGE ( 'NONE', *, *, #2747, .F. ) ;
#5541=EDGE_LOOP ( 'NONE', ( #1482, #3311, #725, #4718 ) ) ;
#5545=EDGE_LOOP ( 'NONE', ( #3963, #1955 ) ) ;
#5553=ORIENTED_EDGE ( 'NONE', *, *, #8262, .F. ) ;
#5566=ADVANCED_FACE ( 'NONE', ( #7089 ), #5817, .F. ) ;
#5581=ORIENTED_EDGE ( 'NONE', *, *, #7913, .T. ) ;
#5651=CYLINDRICAL_SURFACE ( 'NONE', #6663, 2.649999999999993694 ) ;
#5653=ORIENTED_EDGE ( 'NONE', *, *, #7670, .F. ) ;
#5654=DIRECTION ( 'NONE',  ( 1.000000000000000000, 0.000000000000000000, 0.000000000000000000 ) ) ;
#5659=ORIENTED_EDGE ( 'NONE', *, *, #5178, .F. ) ;
#5675=DIRECTION ( 'NONE',  ( 0.000000000000000000, 1.000000000000000000, 0.000000000000000000 ) ) ;
#5701=ADVANCED_FACE ( 'NONE', ( #1338 ), #6601, .F. ) ;
#5764=DIRECTION ( 'NONE',  ( 1.000000000000000000, 0.000000000000000000, 0.000000000000000000 ) ) ;
#5768=DIRECTION ( 'NONE',  ( 1.000000000000000000, 0.000000000000000000, 0.000000000000000000 ) ) ;
#5788=VERTEX_POINT ( 'NONE', #2906 ) ;
#5794=FACE_BOUND ( 'NONE', #5545, .T. ) ;
#5801=CARTESIAN_POINT ( 'NONE',  ( -20.00000000000000000, 175.0000000000000284, 0.000000000000000000 ) ) ;
#5817=CYLINDRICAL_SURFACE ( 'NONE', #6434, 2.649999999999993694 ) ;
#5822=ORIENTED_EDGE ( 'NONE', *, *, #4313, .T. ) ;
#5867=LINE ( 'NONE', #8540, #8057 ) ;
#5872=LINE ( 'NONE', #8069, #5999 ) ;
#5877=LINE ( 'NONE', #3237, #3744 ) ;
#5887=ORIENTED_EDGE ( 'NONE', *, *, #6089, .F. ) ;
#5901=ORIENTED_EDGE ( 'NONE', *, *, #3426, .F. ) ;
#5914=CARTESIAN_POINT ( 'NONE',  ( -20.00000000000000000, 175.0000000000000284, 5.000000000000000000 ) ) ;
#5915=ORIENTED_EDGE ( 'NONE', *, *, #8595, .F. ) ;
#5920=CIRCLE ( 'NONE', #5098, 2.649999999999987477 ) ;
#5921=ADVANCED_FACE ( 'NONE', ( #4952 ), #6426, .F. ) ;
#5938=DIRECTION ( 'NONE',  ( 1.000000000000000000, 0.000000000000000000, 0.000000000000000000 ) ) ;
#5953=DIRECTION ( 'NONE',  ( 0.000000000000000000, 0.000000000000000000, 1.000000000000000000 ) ) ;
#5991=CARTESIAN_POINT ( 'NONE',  ( -4.999999999999998224, 135.0000000000000000, 15.00000000000000355 ) ) ;
#5999=VECTOR ( 'NONE', #5953, 1000.000000000000000 ) ;
#6089=EDGE_CURVE ( 'NONE', #4430, #6694, #8563, .T. ) ;
#6095=CARTESIAN_POINT ( 'NONE',  ( 20.00000000000000000, 175.0000000000000284, 0.000000000000000000 ) ) ;
#6097=VERTEX_POINT ( 'NONE', #7825 ) ;
#6108=DIRECTION ( 'NONE',  ( 0.000000000000000000, 0.000000000000000000, -1.000000000000000000 ) ) ;
#6159=ORIENTED_EDGE ( 'NONE', *, *, #7490, .F. ) ;
#6163=EDGE_LOOP ( 'NONE', ( #6377, #2538, #633, #5211 ) ) ;
#6172=EDGE_LOOP ( 'NONE', ( #962, #3668, #8221, #1150 ) ) ;
#6228=( NAMED_UNIT ( * ) SI_UNIT ( $, .STERADIAN. ) SOLID_ANGLE_UNIT ( ) );
#6256=PLANE ( 'NONE',  #8566 ) ;
#6300=FACE_OUTER_BOUND ( 'NONE', #1526, .T. ) ;
#6317=CARTESIAN_POINT ( 'NONE',  ( 20.00000000000000000, 135.0000000000000000, 40.00000000000000000 ) ) ;
#6319=EDGE_CURVE ( 'NONE', #4430, #5788, #7602, .T. ) ;
#6341=CARTESIAN_POINT ( 'NONE',  ( 5.000000000000001776, 140.0000000000000000, 15.00000000000000355 ) ) ;
#6343=VECTOR ( 'NONE', #1397, 1000.000000000000000 ) ;
#6377=ORIENTED_EDGE ( 'NONE', *, *, #2295, .F. ) ;
#6378=ADVANCED_FACE ( 'NONE', ( #7691 ), #4287, .F. ) ;
#6396=CARTESIAN_POINT ( 'NONE',  ( 20.00000000000000000, 140.0000000000000000, 40.00000000000000000 ) ) ;
#6405=CARTESIAN_POINT ( 'NONE',  ( 20.00000000000000000, 140.0000000000000000, 40.00000000000000000 ) ) ;
#6426=PLANE ( 'NONE',  #632 ) ;
#6434=AXIS2_PLACEMENT_3D ( 'NONE', #1662, #343, #5654 ) ;
#6451=DIRECTION ( 'NONE',  ( -1.000000000000000000, 0.000000000000000000, -0.000000000000000000 ) ) ;
#6456=ORIENTED_EDGE ( 'NONE', *, *, #3426, .T. ) ;
#6464=EDGE_LOOP ( 'NONE', ( #5659, #1918, #7963, #5512 ) ) ;
#6485=LINE ( 'NONE', #5136, #4111 ) ;
#6488=EDGE_LOOP ( 'NONE', ( #5017, #4638 ) ) ;
#6511=VECTOR ( 'NONE', #5264, 1000.000000000000000 ) ;
#6531=PLANE ( 'NONE',  #3852 ) ;
#6545=LINE ( 'NONE', #593, #1024 ) ;
#6563=CARTESIAN_POINT ( 'NONE',  ( -20.00000000000000000, 135.0000000000000000, 0.000000000000000000 ) ) ;
#6586=CARTESIAN_POINT ( 'NONE',  ( -20.00000000000000000, 140.0000000000000000, 40.00000000000000000 ) ) ;
#6601=PLANE ( 'NONE',  #7830 ) ;
#6625=FACE_OUTER_BOUND ( 'NONE', #6172, .T. ) ;
#6627=DIRECTION ( 'NONE',  ( 1.000000000000000000, 0.000000000000000000, 0.000000000000000000 ) ) ;
#6663=AXIS2_PLACEMENT_3D ( 'NONE', #3784, #999, #5084 ) ;
#6668=SURFACE_SIDE_STYLE ('',( #1366 ) ) ;
#6678=LINE ( 'NONE', #726, #1016 ) ;
#6694=VERTEX_POINT ( 'NONE', #4922 ) ;
#6702=FACE_OUTER_BOUND ( 'NONE', #7171, .T. ) ;
#6726=DIRECTION ( 'NONE',  ( -1.000000000000000000, 0.000000000000000000, 0.000000000000000000 ) ) ;
#6761=VERTEX_POINT ( 'NONE', #6396 ) ;
#6780=LINE ( 'NONE', #2173, #1373 ) ;
#6782=LINE ( 'NONE', #7483, #1642 ) ;
#6801=ORIENTED_EDGE ( 'NONE', *, *, #8466, .F. ) ;
#6802=ORIENTED_EDGE ( 'NONE', *, *, #2896, .T. ) ;
#6822=LINE ( 'NONE', #2828, #6931 ) ;
#6874=ORIENTED_EDGE ( 'NONE', *, *, #6319, .F. ) ;
#6931=VECTOR ( 'NONE', #2268, 1000.000000000000000 ) ;
#6936=CARTESIAN_POINT ( 'NONE',  ( 2.649999999999993694, 157.5000000000000284, 5.000000000000000000 ) ) ;
#6940=ORIENTED_EDGE ( 'NONE', *, *, #1895, .T. ) ;
#7021=DIRECTION ( 'NONE',  ( -0.000000000000000000, -0.000000000000000000, -1.000000000000000000 ) ) ;
#7068=PLANE ( 'NONE',  #2729 ) ;
#7089=FACE_OUTER_BOUND ( 'NONE', #5138, .T. ) ;
#7102=DIRECTION ( 'NONE',  ( -0.000000000000000000, 0.000000000000000000, -1.000000000000000000 ) ) ;
#7171=EDGE_LOOP ( 'NONE', ( #5887, #5901, #6940, #5095 ) ) ;
#7260=VECTOR ( 'NONE', #707, 1000.000000000000000 ) ;
#7317=AXIS2_PLACEMENT_3D ( 'NONE', #5509, #2209, #4206 ) ;
#7334=FILL_AREA_STYLE ('',( #4672 ) ) ;
#7339=LINE ( 'NONE', #4032, #7836 ) ;
#7341=CARTESIAN_POINT ( 'NONE',  ( 20.00000000000000000, 175.0000000000000284, 5.000000000000000000 ) ) ;
#7343=CARTESIAN_POINT ( 'NONE',  ( -4.999999999999998224, 140.0000000000000000, 15.00000000000000355 ) ) ;
#7393=PRODUCT ( 'single rail^MAS-188', 'single rail^MAS-188', '', ( #3215 ) ) ;
#7395=ORIENTED_EDGE ( 'NONE', *, *, #8595, .T. ) ;
#7404=LINE ( 'NONE', #5914, #1928 ) ;
#7406=FACE_OUTER_BOUND ( 'NONE', #8374, .T. ) ;
#7481=DIRECTION ( 'NONE',  ( -0.000000000000000000, -0.000000000000000000, 1.000000000000000000 ) ) ;
#7483=CARTESIAN_POINT ( 'NONE',  ( -20.00000000000000000, 175.0000000000000284, 0.000000000000000000 ) ) ;
#7490=EDGE_CURVE ( 'NONE', #3102, #5372, #6545, .T. ) ;
#7523=EDGE_CURVE ( 'NONE', #6097, #3102, #7339, .T. ) ;
#7543=VECTOR ( 'NONE', #5433, 1000.000000000000000 ) ;
#7561=VERTEX_POINT ( 'NONE', #8133 ) ;
#7577=ORIENTED_EDGE ( 'NONE', *, *, #4278, .F. ) ;
#7602=LINE ( 'NONE', #4243, #2436 ) ;
#7604=VECTOR ( 'NONE', #6627, 1000.000000000000000 ) ;
#7642=VECTOR ( 'NONE', #2616, 1000.000000000000000 ) ;
#7656=VECTOR ( 'NONE', #4546, 1000.000000000000000 ) ;
#7662=CARTESIAN_POINT ( 'NONE',  ( 5.000000000000000000, 140.0000000000000000, 25.00000000000000000 ) ) ;
#7670=EDGE_CURVE ( 'NONE', #530, #3740, #276, .T. ) ;
#7691=FACE_OUTER_BOUND ( 'NONE', #436, .T. ) ;
#7701=FACE_OUTER_BOUND ( 'NONE', #8075, .T. ) ;
#7747=MECHANICAL_DESIGN_GEOMETRIC_PRESENTATION_REPRESENTATION('',(#8164),#1342);
#7764=APPLICATION_CONTEXT ( 'automotive_design' ) ;
#7776=VECTOR ( 'NONE', #3047, 1000.000000000000000 ) ;
#7825=CARTESIAN_POINT ( 'NONE',  ( -4.999999999999998224, 135.0000000000000000, 15.00000000000000355 ) ) ;
#7830=AXIS2_PLACEMENT_3D ( 'NONE', #4005, #8011, #25 ) ;
#7836=VECTOR ( 'NONE', #2642, 1000.000000000000000 ) ;
#7842=AXIS2_PLACEMENT_3D ( 'NONE', #1681, #4375, #3722 ) ;
#7843=CARTESIAN_POINT ( 'NONE',  ( 0.000000000000000000, 157.5000000000000284, 0.000000000000000000 ) ) ;
#7850=FACE_OUTER_BOUND ( 'NONE', #1295, .T. ) ;
#7866=PRODUCT_DEFINITION_CONTEXT ( 'detailed design', #1081, 'design' ) ;
#7888=CIRCLE ( 'NONE', #3030, 2.649999999999987477 ) ;
#7913=EDGE_CURVE ( 'NONE', #5372, #3043, #1899, .T. ) ;
#7916=LINE ( 'NONE', #1958, #8378 ) ;
#7922=AXIS2_PLACEMENT_3D ( 'NONE', #7984, #620, #8030 ) ;
#7958=DIRECTION ( 'NONE',  ( 0.000000000000000000, 1.000000000000000000, 0.000000000000000000 ) ) ;
#7963=ORIENTED_EDGE ( 'NONE', *, *, #2896, .F. ) ;
#7969=VECTOR ( 'NONE', #7975, 1000.000000000000000 ) ;
#7975=DIRECTION ( 'NONE',  ( -0.000000000000000000, 1.000000000000000000, -0.000000000000000000 ) ) ;
#7984=CARTESIAN_POINT ( 'NONE',  ( 0.000000000000000000, 0.000000000000000000, 40.00000000000000000 ) ) ;
#7998=ORIENTED_EDGE ( 'NONE', *, *, #4213, .T. ) ;
#8001=DIRECTION ( 'NONE',  ( -1.734723475976807587E-16, 0.000000000000000000, 1.000000000000000000 ) ) ;
#8011=DIRECTION ( 'NONE',  ( -1.000000000000000000, 0.000000000000000000, 0.000000000000000000 ) ) ;
#8030=DIRECTION ( 'NONE',  ( -1.000000000000000000, 0.000000000000000000, -0.000000000000000000 ) ) ;
#8057=VECTOR ( 'NONE', #738, 1000.000000000000000 ) ;
#8069=CARTESIAN_POINT ( 'NONE',  ( -4.999999999999998224, 140.0000000000000000, 15.00000000000000355 ) ) ;
#8075=EDGE_LOOP ( 'NONE', ( #1971, #5915, #6801, #7998 ) ) ;
#8076=DIRECTION ( 'NONE',  ( 0.000000000000000000, -0.000000000000000000, 1.000000000000000000 ) ) ;
#8098=VERTEX_POINT ( 'NONE', #266 ) ;
#8103=DIRECTION ( 'NONE',  ( -1.000000000000000000, 0.000000000000000000, -0.000000000000000000 ) ) ;
#8133=CARTESIAN_POINT ( 'NONE',  ( -20.00000000000000000, 135.0000000000000000, 0.000000000000000000 ) ) ;
#8158=CARTESIAN_POINT ( 'NONE',  ( 2.649999999999987477, 157.5000000000000284, 5.000000000000000888 ) ) ;
#8164=STYLED_ITEM('',(#8657),#2129);
#8182=CARTESIAN_POINT ( 'NONE',  ( 20.00000000000000000, 140.0000000000000000, 40.00000000000000000 ) ) ;
#8221=ORIENTED_EDGE ( 'NONE', *, *, #3084, .T. ) ;
#8258=ORIENTED_EDGE ( 'NONE', *, *, #2851, .T. ) ;
#8262=EDGE_CURVE ( 'NONE', #1426, #3213, #2180, .T. ) ;
#8315=VERTEX_POINT ( 'NONE', #4265 ) ;
#8370=DIRECTION ( 'NONE',  ( -0.000000000000000000, 1.000000000000000000, -0.000000000000000000 ) ) ;
#8374=EDGE_LOOP ( 'NONE', ( #252, #474, #3741, #5468 ) ) ;
#8378=VECTOR ( 'NONE', #1877, 1000.000000000000000 ) ;
#8380=DIRECTION ( 'NONE',  ( 0.000000000000000000, 0.000000000000000000, -1.000000000000000000 ) ) ;
#8403=VECTOR ( 'NONE', #1251, 1000.000000000000000 ) ;
#8421=VERTEX_POINT ( 'NONE', #7343 ) ;
#8463=ORIENTED_EDGE ( 'NONE', *, *, #7490, .T. ) ;
#8466=EDGE_CURVE ( 'NONE', #8098, #5082, #3299, .T. ) ;
#8499=( NAMED_UNIT ( * ) PLANE_ANGLE_UNIT ( ) SI_UNIT ( $, .RADIAN. ) );
#8502=CARTESIAN_POINT ( 'NONE',  ( 2.649999999999993694, 157.5000000000000284, 0.000000000000000000 ) ) ;
#8533=VERTEX_POINT ( 'NONE', #193 ) ;
#8540=CARTESIAN_POINT ( 'NONE',  ( -4.999999999999998224, 140.0000000000000000, 25.00000000000000000 ) ) ;
#8547=EDGE_CURVE ( 'NONE', #530, #3444, #1159, .T. ) ;
#8563=LINE ( 'NONE', #3951, #7656 ) ;
#8566=AXIS2_PLACEMENT_3D ( 'NONE', #4956, #867, #8103 ) ;
#8591=DIRECTION ( 'NONE',  ( -0.000000000000000000, -0.000000000000000000, 1.000000000000000000 ) ) ;
#8595=EDGE_CURVE ( 'NONE', #5082, #3699, #6678, .T. ) ;
#8651=COLOUR_RGB('Sky Blue',0.24,0.69,0.87);
#8652=FILL_AREA_STYLE_COLOUR('',#8651);
#8653=FILL_AREA_STYLE('',(#8652));
#8654=SURFACE_STYLE_FILL_AREA(#8653);
#8655=SURFACE_SIDE_STYLE('',(#8654));
#8656=SURFACE_STYLE_USAGE(.BOTH.,#8655);
#8657=PRESENTATION_STYLE_ASSIGNMENT((#8656));
ENDSEC;
END-ISO-10303-21;
